ISO-10303-21;
HEADER;
/* Generated by software containing ST-Developer
 * from STEP Tools, Inc. (www.steptools.com) 
 */

FILE_DESCRIPTION(
/* description */ ('Cable chain and bracket set'),
/* implementation_level */ '2;1');

FILE_NAME(
/* name */ 'Flat Washer - M6__PD6070.step',
/* time_stamp */ '2026-10-29T17:19:47-07:00',
/* author */ (''),
/* organization */ (''),
/* preprocessor_version */ 'ST-DEVELOPER v20.2',
/* originating_system */ 'Autodesk Translation Framework v15.17.0.0',
/* authorisation */ '');

FILE_SCHEMA (('AUTOMOTIVE_DESIGN { 1 0 10303 214 3 1 1 }'));
ENDSEC;

DATA;
#10=MECHANICAL_DESIGN_GEOMETRIC_PRESENTATION_REPRESENTATION('',(#341),#5929);
#315=SHAPE_REPRESENTATION_RELATIONSHIP('SRR','None',#6046,#328);
#328=ADVANCED_BREP_SHAPE_REPRESENTATION('',(#354),#5913);
#341=STYLED_ITEM('',(#6227),#354);
#354=MANIFOLD_SOLID_BREP('Body1',#3335);
#379=FACE_BOUND('',#802,.T.);
#380=FACE_BOUND('',#804,.T.);
#455=PLANE('',#3564);
#456=PLANE('',#3565);
#601=FACE_OUTER_BOUND('',#799,.T.);
#602=FACE_OUTER_BOUND('',#800,.T.);
#603=FACE_OUTER_BOUND('',#801,.T.);
#604=FACE_OUTER_BOUND('',#803,.T.);
#799=EDGE_LOOP('',(#2605,#2606,#2607,#2608));
#800=EDGE_LOOP('',(#2609,#2610,#2611,#2612));
#801=EDGE_LOOP('',(#2613));
#802=EDGE_LOOP('',(#2614));
#803=EDGE_LOOP('',(#2615));
#804=EDGE_LOOP('',(#2616));
#1051=LINE('',#5244,#1311);
#1052=LINE('',#5250,#1312);
#1311=VECTOR('',#4208,0.320000000000037);
#1312=VECTOR('',#4215,0.600000000000068);
#1497=CIRCLE('',#3559,0.320000000000037);
#1498=CIRCLE('',#3560,0.320000000000037);
#1499=CIRCLE('',#3562,0.600000000000069);
#1500=CIRCLE('',#3563,0.600000000000069);
#1671=VERTEX_POINT('',#5241);
#1672=VERTEX_POINT('',#5243);
#1673=VERTEX_POINT('',#5247);
#1674=VERTEX_POINT('',#5249);
#2003=EDGE_CURVE('',#1671,#1671,#1497,.T.);
#2004=EDGE_CURVE('',#1671,#1672,#1051,.T.);
#2005=EDGE_CURVE('',#1672,#1672,#1498,.T.);
#2006=EDGE_CURVE('',#1673,#1673,#1499,.T.);
#2007=EDGE_CURVE('',#1673,#1674,#1052,.T.);
#2008=EDGE_CURVE('',#1674,#1674,#1500,.T.);
#2605=ORIENTED_EDGE('',*,*,#2003,.F.);
#2606=ORIENTED_EDGE('',*,*,#2004,.T.);
#2607=ORIENTED_EDGE('',*,*,#2005,.T.);
#2608=ORIENTED_EDGE('',*,*,#2004,.F.);
#2609=ORIENTED_EDGE('',*,*,#2006,.F.);
#2610=ORIENTED_EDGE('',*,*,#2007,.T.);
#2611=ORIENTED_EDGE('',*,*,#2008,.T.);
#2612=ORIENTED_EDGE('',*,*,#2007,.F.);
#2613=ORIENTED_EDGE('',*,*,#2006,.T.);
#2614=ORIENTED_EDGE('',*,*,#2003,.T.);
#2615=ORIENTED_EDGE('',*,*,#2008,.F.);
#2616=ORIENTED_EDGE('',*,*,#2005,.F.);
#3119=CYLINDRICAL_SURFACE('',#3558,0.320000000000037);
#3120=CYLINDRICAL_SURFACE('',#3561,0.600000000000069);
#3223=ADVANCED_FACE('',(#601),#3119,.F.);
#3224=ADVANCED_FACE('',(#602),#3120,.T.);
#3225=ADVANCED_FACE('',(#603,#379),#455,.T.);
#3226=ADVANCED_FACE('',(#604,#380),#456,.F.);
#3335=CLOSED_SHELL('',(#3223,#3224,#3225,#3226));
#3557=AXIS2_PLACEMENT_3D('',#5239,#4202,#4203);
#3558=AXIS2_PLACEMENT_3D('',#5240,#4204,#4205);
#3559=AXIS2_PLACEMENT_3D('',#5242,#4206,#4207);
#3560=AXIS2_PLACEMENT_3D('',#5245,#4209,#4210);
#3561=AXIS2_PLACEMENT_3D('',#5246,#4211,#4212);
#3562=AXIS2_PLACEMENT_3D('',#5248,#4213,#4214);
#3563=AXIS2_PLACEMENT_3D('',#5251,#4216,#4217);
#3564=AXIS2_PLACEMENT_3D('',#5252,#4218,#4219);
#3565=AXIS2_PLACEMENT_3D('',#5253,#4220,#4221);
#4202=DIRECTION('axis',(0.,0.,1.));
#4203=DIRECTION('refdir',(1.,0.,0.));
#4204=DIRECTION('center_axis',(-6.12323399573548E-17,1.,4.78224871431377E-30));
#4205=DIRECTION('ref_axis',(0.939692587475203,5.75395759716863E-17,0.342020234846066));
#4206=DIRECTION('center_axis',(6.12323399573548E-17,-1.,-4.78224871431377E-30));
#4207=DIRECTION('ref_axis',(0.939692587475203,5.75395759716863E-17,0.342020234846066));
#4208=DIRECTION('',(6.12323399573548E-17,-1.,-4.78224871431377E-30));
#4209=DIRECTION('center_axis',(6.12323399573548E-17,-1.,-4.78224871431377E-30));
#4210=DIRECTION('ref_axis',(0.939692587475203,5.75395759716863E-17,0.342020234846066));
#4211=DIRECTION('center_axis',(-6.12323399573548E-17,1.,4.78224871431377E-30));
#4212=DIRECTION('ref_axis',(0.939692587475203,5.75395759716863E-17,0.342020234846066));
#4213=DIRECTION('center_axis',(-6.12323399573548E-17,1.,4.78224871431377E-30));
#4214=DIRECTION('ref_axis',(0.939692587475203,5.75395759716863E-17,0.342020234846066));
#4215=DIRECTION('',(6.12323399573548E-17,-1.,-4.78224871431377E-30));
#4216=DIRECTION('center_axis',(-6.12323399573548E-17,1.,4.78224871431377E-30));
#4217=DIRECTION('ref_axis',(0.939692587475203,5.75395759716863E-17,0.342020234846066));
#4218=DIRECTION('center_axis',(-6.12323399573548E-17,1.,4.78224871431377E-30));
#4219=DIRECTION('ref_axis',(0.939692587475203,5.75395759716863E-17,0.342020234846066));
#4220=DIRECTION('center_axis',(-6.12323399573548E-17,1.,4.78224871431377E-30));
#4221=DIRECTION('ref_axis',(0.939692587475203,5.75395759716863E-17,0.342020234846066));
#5239=CARTESIAN_POINT('',(0.,0.,0.));
#5240=CARTESIAN_POINT('Origin',(2.34923146868827,1.56,3.85505058711526));
#5241=CARTESIAN_POINT('',(2.04852984069618,1.72000000000002,3.74560411196451));
#5242=CARTESIAN_POINT('Origin',(2.34923146868827,1.72000000000002,3.85505058711526));
#5243=CARTESIAN_POINT('',(2.04852984069618,1.56,3.74560411196451));
#5244=CARTESIAN_POINT('',(2.04852984069618,1.56,3.74560411196451));
#5245=CARTESIAN_POINT('Origin',(2.34923146868827,1.56,3.85505058711526));
#5246=CARTESIAN_POINT('Origin',(2.34923146868827,1.56,3.85505058711526));
#5247=CARTESIAN_POINT('',(1.78541591620309,1.72000000000002,3.6498384462076));
#5248=CARTESIAN_POINT('Origin',(2.34923146868827,1.72000000000002,3.85505058711526));
#5249=CARTESIAN_POINT('',(1.78541591620309,1.56,3.6498384462076));
#5250=CARTESIAN_POINT('',(1.78541591620309,1.56,3.6498384462076));
#5251=CARTESIAN_POINT('Origin',(2.34923146868827,1.56,3.85505058711526));
#5252=CARTESIAN_POINT('Origin',(2.34923146868827,1.72000000000002,3.85505058711526));
#5253=CARTESIAN_POINT('Origin',(2.34923146868827,1.56,3.85505058711526));
#5889=UNCERTAINTY_MEASURE_WITH_UNIT(LENGTH_MEASURE(0.001),#5930,
'DISTANCE_ACCURACY_VALUE',
'Maximum model space distance between geometric entities at asserted c
onnectivities');
#5905=UNCERTAINTY_MEASURE_WITH_UNIT(LENGTH_MEASURE(0.001),#5930,
'DISTANCE_ACCURACY_VALUE',
'Maximum model space distance between geometric entities at asserted c
onnectivities');
#5913=(
GEOMETRIC_REPRESENTATION_CONTEXT(3)
GLOBAL_UNCERTAINTY_ASSIGNED_CONTEXT((#5889))
GLOBAL_UNIT_ASSIGNED_CONTEXT((#5930,#5932,#5933))
REPRESENTATION_CONTEXT('','3D')
);
#5929=(
GEOMETRIC_REPRESENTATION_CONTEXT(3)
GLOBAL_UNCERTAINTY_ASSIGNED_CONTEXT((#5905))
GLOBAL_UNIT_ASSIGNED_CONTEXT((#5930,#5932,#5933))
REPRESENTATION_CONTEXT('','3D')
);
#5930=(
LENGTH_UNIT()
NAMED_UNIT(*)
SI_UNIT(.CENTI.,.METRE.)
);
#5932=(
NAMED_UNIT(*)
PLANE_ANGLE_UNIT()
SI_UNIT($,.RADIAN.)
);
#5933=(
NAMED_UNIT(*)
SI_UNIT($,.STERADIAN.)
SOLID_ANGLE_UNIT()
);
#5941=SHAPE_DEFINITION_REPRESENTATION(#5964,#6046);
#5964=PRODUCT_DEFINITION_SHAPE('',$,#6070);
#6046=SHAPE_REPRESENTATION('',(#3557),#5913);
#6062=PRODUCT_DEFINITION_CONTEXT('part definition',#6133,'design');
#6070=PRODUCT_DEFINITION('Flat Washer - M6','Flat Washer - M6',#6093,#6062);
#6093=PRODUCT_DEFINITION_FORMATION('',$,#6142);
#6133=APPLICATION_CONTEXT(
'Core Data for Automotive Mechanical Design Process');
#6134=PRODUCT_CONTEXT('part definition',#6133,'mechanical');
#6142=PRODUCT('Flat Washer - M6','Flat Washer - M6','Flat Washer - M6',
(#6134));
#6221=COLOUR_RGB('Black',0.12,0.14,0.17);
#6222=FILL_AREA_STYLE_COLOUR('',#6221);
#6223=FILL_AREA_STYLE('',(#6222));
#6224=SURFACE_STYLE_FILL_AREA(#6223);
#6225=SURFACE_SIDE_STYLE('',(#6224));
#6226=SURFACE_STYLE_USAGE(.BOTH.,#6225);
#6227=PRESENTATION_STYLE_ASSIGNMENT((#6226));
ENDSEC;
END-ISO-10303-21;
